ISO-10303-21;
HEADER;
/* Generated by software containing ST-Developer
 * from STEP Tools, Inc. (www.steptools.com) 
 */

FILE_DESCRIPTION(
/* description */ ('Union bypass pipe loop'),
/* implementation_level */ '2;1');

FILE_NAME(
/* name */ 'Cap Screw - M8x30.step',
/* time_stamp */ '2026-10-27T21:00:29-07:00',
/* author */ (''),
/* organization */ (''),
/* preprocessor_version */ 'ST-DEVELOPER v20.2',
/* originating_system */ 'Autodesk Translation Framework v15.17.0.0',
/* authorisation */ '');

FILE_SCHEMA (('AUTOMOTIVE_DESIGN { 1 0 10303 214 3 1 1 }'));
ENDSEC;

DATA;
#10=MECHANICAL_DESIGN_GEOMETRIC_PRESENTATION_REPRESENTATION('',(#468),#10095);
#363=CONICAL_SURFACE('',#6428,0.625,0.785398163397448);
#364=CONICAL_SURFACE('',#6432,0.635,0.785398163397449);
#365=CONICAL_SURFACE('',#6436,0.41,0.463647609000806);
#366=CONICAL_SURFACE('',#6440,0.36,0.785398163397448);
#374=ORIENTED_CLOSED_SHELL('',*,#5542,.F.);
#378=BREP_WITH_VOIDS('Body1',#5541,(#374));
#404=SHAPE_REPRESENTATION_RELATIONSHIP('SRR','None',#10273,#436);
#436=ADVANCED_BREP_SHAPE_REPRESENTATION('',(#378),#10085);
#468=STYLED_ITEM('',(#10507),#378);
#621=FACE_BOUND('',#1517,.T.);
#760=PLANE('',#6426);
#761=PLANE('',#6434);
#762=PLANE('',#6442);
#763=PLANE('',#6443);
#764=PLANE('',#6444);
#765=PLANE('',#6445);
#766=PLANE('',#6446);
#767=PLANE('',#6447);
#768=PLANE('',#6448);
#769=PLANE('',#6449);
#770=PLANE('',#6450);
#1070=FACE_OUTER_BOUND('',#1512,.T.);
#1071=FACE_OUTER_BOUND('',#1513,.T.);
#1072=FACE_OUTER_BOUND('',#1514,.T.);
#1073=FACE_OUTER_BOUND('',#1515,.T.);
#1074=FACE_OUTER_BOUND('',#1516,.T.);
#1075=FACE_OUTER_BOUND('',#1518,.T.);
#1076=FACE_OUTER_BOUND('',#1519,.T.);
#1077=FACE_OUTER_BOUND('',#1520,.T.);
#1078=FACE_OUTER_BOUND('',#1521,.T.);
#1079=FACE_OUTER_BOUND('',#1522,.T.);
#1080=FACE_OUTER_BOUND('',#1523,.T.);
#1081=FACE_OUTER_BOUND('',#1524,.T.);
#1082=FACE_OUTER_BOUND('',#1525,.T.);
#1083=FACE_OUTER_BOUND('',#1526,.T.);
#1084=FACE_OUTER_BOUND('',#1527,.T.);
#1085=FACE_OUTER_BOUND('',#1528,.T.);
#1086=FACE_OUTER_BOUND('',#1529,.T.);
#1512=EDGE_LOOP('',(#4684));
#1513=EDGE_LOOP('',(#4685,#4686,#4687,#4688));
#1514=EDGE_LOOP('',(#4689,#4690,#4691,#4692));
#1515=EDGE_LOOP('',(#4693,#4694,#4695,#4696));
#1516=EDGE_LOOP('',(#4697));
#1517=EDGE_LOOP('',(#4698));
#1518=EDGE_LOOP('',(#4699,#4700,#4701,#4702));
#1519=EDGE_LOOP('',(#4703,#4704,#4705,#4706));
#1520=EDGE_LOOP('',(#4707,#4708,#4709,#4710));
#1521=EDGE_LOOP('',(#4711));
#1522=EDGE_LOOP('',(#4712,#4713,#4714,#4715));
#1523=EDGE_LOOP('',(#4716,#4717,#4718,#4719));
#1524=EDGE_LOOP('',(#4720,#4721,#4722,#4723));
#1525=EDGE_LOOP('',(#4724,#4725,#4726,#4727));
#1526=EDGE_LOOP('',(#4728,#4729,#4730,#4731));
#1527=EDGE_LOOP('',(#4732,#4733,#4734,#4735));
#1528=EDGE_LOOP('',(#4736,#4737,#4738,#4739,#4740,#4741));
#1529=EDGE_LOOP('',(#4742,#4743,#4744,#4745,#4746,#4747));
#1860=LINE('',#9533,#2236);
#1861=LINE('',#9537,#2237);
#1862=LINE('',#9541,#2238);
#1863=LINE('',#9548,#2239);
#1864=LINE('',#9552,#2240);
#1865=LINE('',#9556,#2241);
#1866=LINE('',#9561,#2242);
#1867=LINE('',#9563,#2243);
#1868=LINE('',#9565,#2244);
#1869=LINE('',#9566,#2245);
#1870=LINE('',#9569,#2246);
#1871=LINE('',#9571,#2247);
#1872=LINE('',#9572,#2248);
#1873=LINE('',#9575,#2249);
#1874=LINE('',#9577,#2250);
#1875=LINE('',#9578,#2251);
#1876=LINE('',#9581,#2252);
#1877=LINE('',#9583,#2253);
#1878=LINE('',#9584,#2254);
#1879=LINE('',#9587,#2255);
#1880=LINE('',#9589,#2256);
#1881=LINE('',#9590,#2257);
#1882=LINE('',#9592,#2258);
#1883=LINE('',#9593,#2259);
#2236=VECTOR('',#7906,0.625);
#2237=VECTOR('',#7911,0.65);
#2238=VECTOR('',#7916,0.635);
#2239=VECTOR('',#7925,0.41);
#2240=VECTOR('',#7930,0.4);
#2241=VECTOR('',#7935,0.36);
#2242=VECTOR('',#7940,1.);
#2243=VECTOR('',#7941,1.);
#2244=VECTOR('',#7942,1.);
#2245=VECTOR('',#7943,1.);
#2246=VECTOR('',#7946,1.);
#2247=VECTOR('',#7947,1.);
#2248=VECTOR('',#7948,1.);
#2249=VECTOR('',#7951,1.);
#2250=VECTOR('',#7952,1.);
#2251=VECTOR('',#7953,1.);
#2252=VECTOR('',#7956,1.);
#2253=VECTOR('',#7957,1.);
#2254=VECTOR('',#7958,1.);
#2255=VECTOR('',#7961,1.);
#2256=VECTOR('',#7962,1.);
#2257=VECTOR('',#7963,1.);
#2258=VECTOR('',#7966,1.);
#2259=VECTOR('',#7967,1.);
#2583=CIRCLE('',#6427,0.6);
#2584=CIRCLE('',#6429,0.65);
#2585=CIRCLE('',#6431,0.65);
#2586=CIRCLE('',#6433,0.62);
#2587=CIRCLE('',#6435,0.42);
#2588=CIRCLE('',#6437,0.3933);
#2589=CIRCLE('',#6439,0.3933);
#2590=CIRCLE('',#6441,0.32);
#2940=VERTEX_POINT('',#9528);
#2941=VERTEX_POINT('',#9531);
#2942=VERTEX_POINT('',#9535);
#2943=VERTEX_POINT('',#9539);
#2944=VERTEX_POINT('',#9543);
#2945=VERTEX_POINT('',#9546);
#2946=VERTEX_POINT('',#9550);
#2947=VERTEX_POINT('',#9554);
#2948=VERTEX_POINT('',#9559);
#2949=VERTEX_POINT('',#9560);
#2950=VERTEX_POINT('',#9562);
#2951=VERTEX_POINT('',#9564);
#2952=VERTEX_POINT('',#9568);
#2953=VERTEX_POINT('',#9570);
#2954=VERTEX_POINT('',#9574);
#2955=VERTEX_POINT('',#9576);
#2956=VERTEX_POINT('',#9580);
#2957=VERTEX_POINT('',#9582);
#2958=VERTEX_POINT('',#9586);
#2959=VERTEX_POINT('',#9588);
#3540=EDGE_CURVE('',#2940,#2940,#2583,.T.);
#3541=EDGE_CURVE('',#2941,#2941,#2584,.T.);
#3542=EDGE_CURVE('',#2941,#2940,#1860,.T.);
#3543=EDGE_CURVE('',#2942,#2942,#2585,.T.);
#3544=EDGE_CURVE('',#2942,#2941,#1861,.T.);
#3545=EDGE_CURVE('',#2943,#2943,#2586,.T.);
#3546=EDGE_CURVE('',#2943,#2942,#1862,.T.);
#3547=EDGE_CURVE('',#2944,#2944,#2587,.T.);
#3548=EDGE_CURVE('',#2945,#2945,#2588,.F.);
#3549=EDGE_CURVE('',#2945,#2944,#1863,.T.);
#3550=EDGE_CURVE('',#2946,#2946,#2589,.F.);
#3551=EDGE_CURVE('',#2946,#2945,#1864,.T.);
#3552=EDGE_CURVE('',#2947,#2947,#2590,.T.);
#3553=EDGE_CURVE('',#2947,#2946,#1865,.T.);
#3554=EDGE_CURVE('',#2948,#2949,#1866,.T.);
#3555=EDGE_CURVE('',#2949,#2950,#1867,.T.);
#3556=EDGE_CURVE('',#2950,#2951,#1868,.T.);
#3557=EDGE_CURVE('',#2948,#2951,#1869,.T.);
#3558=EDGE_CURVE('',#2949,#2952,#1870,.T.);
#3559=EDGE_CURVE('',#2952,#2953,#1871,.T.);
#3560=EDGE_CURVE('',#2953,#2950,#1872,.T.);
#3561=EDGE_CURVE('',#2952,#2954,#1873,.T.);
#3562=EDGE_CURVE('',#2954,#2955,#1874,.T.);
#3563=EDGE_CURVE('',#2955,#2953,#1875,.T.);
#3564=EDGE_CURVE('',#2954,#2956,#1876,.T.);
#3565=EDGE_CURVE('',#2956,#2957,#1877,.T.);
#3566=EDGE_CURVE('',#2957,#2955,#1878,.T.);
#3567=EDGE_CURVE('',#2956,#2958,#1879,.T.);
#3568=EDGE_CURVE('',#2958,#2959,#1880,.T.);
#3569=EDGE_CURVE('',#2959,#2957,#1881,.T.);
#3570=EDGE_CURVE('',#2958,#2948,#1882,.T.);
#3571=EDGE_CURVE('',#2951,#2959,#1883,.T.);
#4684=ORIENTED_EDGE('',*,*,#3540,.F.);
#4685=ORIENTED_EDGE('',*,*,#3541,.F.);
#4686=ORIENTED_EDGE('',*,*,#3542,.T.);
#4687=ORIENTED_EDGE('',*,*,#3540,.T.);
#4688=ORIENTED_EDGE('',*,*,#3542,.F.);
#4689=ORIENTED_EDGE('',*,*,#3543,.F.);
#4690=ORIENTED_EDGE('',*,*,#3544,.T.);
#4691=ORIENTED_EDGE('',*,*,#3541,.T.);
#4692=ORIENTED_EDGE('',*,*,#3544,.F.);
#4693=ORIENTED_EDGE('',*,*,#3545,.F.);
#4694=ORIENTED_EDGE('',*,*,#3546,.T.);
#4695=ORIENTED_EDGE('',*,*,#3543,.T.);
#4696=ORIENTED_EDGE('',*,*,#3546,.F.);
#4697=ORIENTED_EDGE('',*,*,#3545,.T.);
#4698=ORIENTED_EDGE('',*,*,#3547,.F.);
#4699=ORIENTED_EDGE('',*,*,#3548,.F.);
#4700=ORIENTED_EDGE('',*,*,#3549,.T.);
#4701=ORIENTED_EDGE('',*,*,#3547,.T.);
#4702=ORIENTED_EDGE('',*,*,#3549,.F.);
#4703=ORIENTED_EDGE('',*,*,#3550,.F.);
#4704=ORIENTED_EDGE('',*,*,#3551,.T.);
#4705=ORIENTED_EDGE('',*,*,#3548,.T.);
#4706=ORIENTED_EDGE('',*,*,#3551,.F.);
#4707=ORIENTED_EDGE('',*,*,#3552,.F.);
#4708=ORIENTED_EDGE('',*,*,#3553,.T.);
#4709=ORIENTED_EDGE('',*,*,#3550,.T.);
#4710=ORIENTED_EDGE('',*,*,#3553,.F.);
#4711=ORIENTED_EDGE('',*,*,#3552,.T.);
#4712=ORIENTED_EDGE('',*,*,#3554,.T.);
#4713=ORIENTED_EDGE('',*,*,#3555,.T.);
#4714=ORIENTED_EDGE('',*,*,#3556,.T.);
#4715=ORIENTED_EDGE('',*,*,#3557,.F.);
#4716=ORIENTED_EDGE('',*,*,#3558,.T.);
#4717=ORIENTED_EDGE('',*,*,#3559,.T.);
#4718=ORIENTED_EDGE('',*,*,#3560,.T.);
#4719=ORIENTED_EDGE('',*,*,#3555,.F.);
#4720=ORIENTED_EDGE('',*,*,#3561,.T.);
#4721=ORIENTED_EDGE('',*,*,#3562,.T.);
#4722=ORIENTED_EDGE('',*,*,#3563,.T.);
#4723=ORIENTED_EDGE('',*,*,#3559,.F.);
#4724=ORIENTED_EDGE('',*,*,#3564,.T.);
#4725=ORIENTED_EDGE('',*,*,#3565,.T.);
#4726=ORIENTED_EDGE('',*,*,#3566,.T.);
#4727=ORIENTED_EDGE('',*,*,#3562,.F.);
#4728=ORIENTED_EDGE('',*,*,#3567,.T.);
#4729=ORIENTED_EDGE('',*,*,#3568,.T.);
#4730=ORIENTED_EDGE('',*,*,#3569,.T.);
#4731=ORIENTED_EDGE('',*,*,#3565,.F.);
#4732=ORIENTED_EDGE('',*,*,#3570,.T.);
#4733=ORIENTED_EDGE('',*,*,#3557,.T.);
#4734=ORIENTED_EDGE('',*,*,#3571,.T.);
#4735=ORIENTED_EDGE('',*,*,#3568,.F.);
#4736=ORIENTED_EDGE('',*,*,#3570,.F.);
#4737=ORIENTED_EDGE('',*,*,#3567,.F.);
#4738=ORIENTED_EDGE('',*,*,#3564,.F.);
#4739=ORIENTED_EDGE('',*,*,#3561,.F.);
#4740=ORIENTED_EDGE('',*,*,#3558,.F.);
#4741=ORIENTED_EDGE('',*,*,#3554,.F.);
#4742=ORIENTED_EDGE('',*,*,#3571,.F.);
#4743=ORIENTED_EDGE('',*,*,#3556,.F.);
#4744=ORIENTED_EDGE('',*,*,#3560,.F.);
#4745=ORIENTED_EDGE('',*,*,#3563,.F.);
#4746=ORIENTED_EDGE('',*,*,#3566,.F.);
#4747=ORIENTED_EDGE('',*,*,#3569,.F.);
#5172=CYLINDRICAL_SURFACE('',#6430,0.65);
#5173=CYLINDRICAL_SURFACE('',#6438,0.3933);
#5419=ADVANCED_FACE('',(#1070),#760,.T.);
#5420=ADVANCED_FACE('',(#1071),#363,.T.);
#5421=ADVANCED_FACE('',(#1072),#5172,.T.);
#5422=ADVANCED_FACE('',(#1073),#364,.T.);
#5423=ADVANCED_FACE('',(#1074,#621),#761,.T.);
#5424=ADVANCED_FACE('',(#1075),#365,.T.);
#5425=ADVANCED_FACE('',(#1076),#5173,.T.);
#5426=ADVANCED_FACE('',(#1077),#366,.T.);
#5427=ADVANCED_FACE('',(#1078),#762,.T.);
#5428=ADVANCED_FACE('',(#1079),#763,.F.);
#5429=ADVANCED_FACE('',(#1080),#764,.F.);
#5430=ADVANCED_FACE('',(#1081),#765,.F.);
#5431=ADVANCED_FACE('',(#1082),#766,.F.);
#5432=ADVANCED_FACE('',(#1083),#767,.F.);
#5433=ADVANCED_FACE('',(#1084),#768,.F.);
#5434=ADVANCED_FACE('',(#1085),#769,.F.);
#5435=ADVANCED_FACE('',(#1086),#770,.F.);
#5541=CLOSED_SHELL('',(#5419,#5420,#5421,#5422,#5423,#5424,#5425,#5426,
#5427));
#5542=CLOSED_SHELL('',(#5428,#5429,#5430,#5431,#5432,#5433,#5434,#5435));
#6425=AXIS2_PLACEMENT_3D('',#9526,#7896,#7897);
#6426=AXIS2_PLACEMENT_3D('',#9527,#7898,#7899);
#6427=AXIS2_PLACEMENT_3D('',#9529,#7900,#7901);
#6428=AXIS2_PLACEMENT_3D('',#9530,#7902,#7903);
#6429=AXIS2_PLACEMENT_3D('',#9532,#7904,#7905);
#6430=AXIS2_PLACEMENT_3D('',#9534,#7907,#7908);
#6431=AXIS2_PLACEMENT_3D('',#9536,#7909,#7910);
#6432=AXIS2_PLACEMENT_3D('',#9538,#7912,#7913);
#6433=AXIS2_PLACEMENT_3D('',#9540,#7914,#7915);
#6434=AXIS2_PLACEMENT_3D('',#9542,#7917,#7918);
#6435=AXIS2_PLACEMENT_3D('',#9544,#7919,#7920);
#6436=AXIS2_PLACEMENT_3D('',#9545,#7921,#7922);
#6437=AXIS2_PLACEMENT_3D('',#9547,#7923,#7924);
#6438=AXIS2_PLACEMENT_3D('',#9549,#7926,#7927);
#6439=AXIS2_PLACEMENT_3D('',#9551,#7928,#7929);
#6440=AXIS2_PLACEMENT_3D('',#9553,#7931,#7932);
#6441=AXIS2_PLACEMENT_3D('',#9555,#7933,#7934);
#6442=AXIS2_PLACEMENT_3D('',#9557,#7936,#7937);
#6443=AXIS2_PLACEMENT_3D('',#9558,#7938,#7939);
#6444=AXIS2_PLACEMENT_3D('',#9567,#7944,#7945);
#6445=AXIS2_PLACEMENT_3D('',#9573,#7949,#7950);
#6446=AXIS2_PLACEMENT_3D('',#9579,#7954,#7955);
#6447=AXIS2_PLACEMENT_3D('',#9585,#7959,#7960);
#6448=AXIS2_PLACEMENT_3D('',#9591,#7964,#7965);
#6449=AXIS2_PLACEMENT_3D('',#9594,#7968,#7969);
#6450=AXIS2_PLACEMENT_3D('',#9595,#7970,#7971);
#7896=DIRECTION('axis',(0.,0.,1.));
#7897=DIRECTION('refdir',(1.,0.,0.));
#7898=DIRECTION('center_axis',(0.,1.,0.));
#7899=DIRECTION('ref_axis',(0.,0.,1.));
#7900=DIRECTION('center_axis',(0.,-1.,0.));
#7901=DIRECTION('ref_axis',(1.,0.,0.));
#7902=DIRECTION('center_axis',(0.,-1.,0.));
#7903=DIRECTION('ref_axis',(1.,0.,0.));
#7904=DIRECTION('center_axis',(0.,-1.,0.));
#7905=DIRECTION('ref_axis',(1.,0.,0.));
#7906=DIRECTION('',(0.707106781186548,0.707106781186547,8.65956056235493E-17));
#7907=DIRECTION('center_axis',(0.,-1.,0.));
#7908=DIRECTION('ref_axis',(1.,0.,0.));
#7909=DIRECTION('center_axis',(0.,-1.,0.));
#7910=DIRECTION('ref_axis',(1.,0.,0.));
#7911=DIRECTION('',(0.,1.,0.));
#7912=DIRECTION('center_axis',(0.,1.,0.));
#7913=DIRECTION('ref_axis',(1.,0.,0.));
#7914=DIRECTION('center_axis',(0.,-1.,0.));
#7915=DIRECTION('ref_axis',(1.,0.,0.));
#7916=DIRECTION('',(-0.707106781186548,0.707106781186547,-8.65956056235494E-17));
#7917=DIRECTION('center_axis',(0.,-1.,0.));
#7918=DIRECTION('ref_axis',(0.,0.,-1.));
#7919=DIRECTION('center_axis',(0.,-1.,0.));
#7920=DIRECTION('ref_axis',(1.,0.,0.));
#7921=DIRECTION('center_axis',(0.,1.,0.));
#7922=DIRECTION('ref_axis',(1.,0.,0.));
#7923=DIRECTION('center_axis',(0.,1.,0.));
#7924=DIRECTION('ref_axis',(1.,0.,0.));
#7925=DIRECTION('',(-0.447213595499958,0.894427190999916,-5.47678698264203E-17));
#7926=DIRECTION('center_axis',(0.,-1.,0.));
#7927=DIRECTION('ref_axis',(1.,0.,0.));
#7928=DIRECTION('center_axis',(0.,1.,0.));
#7929=DIRECTION('ref_axis',(1.,0.,0.));
#7930=DIRECTION('',(0.,1.,0.));
#7931=DIRECTION('center_axis',(0.,1.,0.));
#7932=DIRECTION('ref_axis',(1.,0.,0.));
#7933=DIRECTION('center_axis',(0.,-1.,0.));
#7934=DIRECTION('ref_axis',(1.,0.,0.));
#7935=DIRECTION('',(-0.707106781186547,0.707106781186548,-8.65956056235493E-17));
#7936=DIRECTION('center_axis',(0.,-1.,0.));
#7937=DIRECTION('ref_axis',(0.,0.,-1.));
#7938=DIRECTION('center_axis',(0.866025403784439,0.,-0.5));
#7939=DIRECTION('ref_axis',(0.5,0.,0.866025403784439));
#7940=DIRECTION('',(-0.5,0.,-0.866025403784439));
#7941=DIRECTION('',(0.,-1.,0.));
#7942=DIRECTION('',(0.5,0.,0.866025403784439));
#7943=DIRECTION('',(0.,-1.,0.));
#7944=DIRECTION('center_axis',(1.60246890531964E-16,0.,-1.));
#7945=DIRECTION('ref_axis',(1.,0.,1.60246890531964E-16));
#7946=DIRECTION('',(-1.,0.,-1.60246890531964E-16));
#7947=DIRECTION('',(0.,-1.,0.));
#7948=DIRECTION('',(1.,0.,1.60246890531964E-16));
#7949=DIRECTION('center_axis',(-0.866025403784439,0.,-0.5));
#7950=DIRECTION('ref_axis',(0.5,0.,-0.866025403784439));
#7951=DIRECTION('',(-0.5,0.,0.866025403784439));
#7952=DIRECTION('',(0.,-1.,0.));
#7953=DIRECTION('',(0.5,0.,-0.866025403784439));
#7954=DIRECTION('center_axis',(-0.866025403784439,0.,0.5));
#7955=DIRECTION('ref_axis',(-0.5,0.,-0.866025403784439));
#7956=DIRECTION('',(0.5,0.,0.866025403784439));
#7957=DIRECTION('',(0.,-1.,0.));
#7958=DIRECTION('',(-0.5,0.,-0.866025403784439));
#7959=DIRECTION('center_axis',(-1.60246890531964E-16,0.,1.));
#7960=DIRECTION('ref_axis',(-1.,0.,-1.60246890531964E-16));
#7961=DIRECTION('',(1.,0.,1.60246890531964E-16));
#7962=DIRECTION('',(0.,-1.,0.));
#7963=DIRECTION('',(-1.,0.,-1.60246890531964E-16));
#7964=DIRECTION('center_axis',(0.866025403784439,0.,0.5));
#7965=DIRECTION('ref_axis',(-0.5,0.,0.866025403784439));
#7966=DIRECTION('',(0.5,0.,-0.866025403784439));
#7967=DIRECTION('',(-0.5,0.,0.866025403784439));
#7968=DIRECTION('center_axis',(0.,1.,0.));
#7969=DIRECTION('ref_axis',(1.,0.,0.));
#7970=DIRECTION('center_axis',(0.,-1.,0.));
#7971=DIRECTION('ref_axis',(0.,0.,-1.));
#9526=CARTESIAN_POINT('',(0.,0.,0.));
#9527=CARTESIAN_POINT('Origin',(0.6,0.8,0.));
#9528=CARTESIAN_POINT('',(-0.6,0.8,-7.34788079488412E-17));
#9529=CARTESIAN_POINT('Origin',(0.,0.8,0.));
#9530=CARTESIAN_POINT('Origin',(0.,0.775,0.));
#9531=CARTESIAN_POINT('',(-0.65,0.75,-7.9602041944578E-17));
#9532=CARTESIAN_POINT('Origin',(0.,0.75,0.));
#9533=CARTESIAN_POINT('',(-0.625,0.775,-7.65404249467096E-17));
#9534=CARTESIAN_POINT('Origin',(0.,0.39,0.));
#9535=CARTESIAN_POINT('',(-0.65,0.0299999999999998,-7.9602041944578E-17));
#9536=CARTESIAN_POINT('Origin',(0.,0.0299999999999998,0.));
#9537=CARTESIAN_POINT('',(-0.65,0.39,-7.9602041944578E-17));
#9538=CARTESIAN_POINT('Origin',(0.,0.0150000000000001,0.));
#9539=CARTESIAN_POINT('',(-0.62,5.89805981832114E-17,-7.59281015471359E-17));
#9540=CARTESIAN_POINT('Origin',(0.,0.,0.));
#9541=CARTESIAN_POINT('',(-0.635,0.0150000000000001,-7.77650717458569E-17));
#9542=CARTESIAN_POINT('Origin',(0.42,0.,0.));
#9543=CARTESIAN_POINT('',(-0.42,-3.46944695195361E-18,-5.14351655641888E-17));
#9544=CARTESIAN_POINT('Origin',(0.,0.,0.));
#9545=CARTESIAN_POINT('Origin',(0.,-0.02,0.));
#9546=CARTESIAN_POINT('',(-0.3933,-0.0534000000000001,4.81653586104654E-17));
#9547=CARTESIAN_POINT('Origin',(0.,-0.0534000000000001,0.));
#9548=CARTESIAN_POINT('',(-0.41,-0.02,-5.02105187650415E-17));
#9549=CARTESIAN_POINT('Origin',(0.,-1.48,0.));
#9550=CARTESIAN_POINT('',(-0.3933,-2.9267,4.81653586104654E-17));
#9551=CARTESIAN_POINT('Origin',(0.,-2.9267,0.));
#9552=CARTESIAN_POINT('',(-0.3933,-1.48,-4.81653586104654E-17));
#9553=CARTESIAN_POINT('Origin',(0.,-2.96,0.));
#9554=CARTESIAN_POINT('',(-0.32,-3.,-3.91886975727153E-17));
#9555=CARTESIAN_POINT('Origin',(0.,-3.,0.));
#9556=CARTESIAN_POINT('',(-0.36,-2.96,-4.40872847693047E-17));
#9557=CARTESIAN_POINT('Origin',(0.,-3.,0.));
#9558=CARTESIAN_POINT('Origin',(0.173205080756888,-0.8,-0.3));
#9559=CARTESIAN_POINT('',(0.346410161513775,-0.8,0.));
#9560=CARTESIAN_POINT('',(0.173205080756888,-0.8,-0.3));
#9561=CARTESIAN_POINT('',(0.346410161513775,-0.8,0.));
#9562=CARTESIAN_POINT('',(0.173205080756888,-1.28,-0.3));
#9563=CARTESIAN_POINT('',(0.173205080756888,-0.8,-0.3));
#9564=CARTESIAN_POINT('',(0.346410161513775,-1.28,0.));
#9565=CARTESIAN_POINT('',(0.346410161513775,-1.28,0.));
#9566=CARTESIAN_POINT('',(0.346410161513775,-0.8,0.));
#9567=CARTESIAN_POINT('Origin',(-0.173205080756888,-0.8,-0.3));
#9568=CARTESIAN_POINT('',(-0.173205080756888,-0.8,-0.3));
#9569=CARTESIAN_POINT('',(0.173205080756888,-0.8,-0.3));
#9570=CARTESIAN_POINT('',(-0.173205080756888,-1.28,-0.3));
#9571=CARTESIAN_POINT('',(-0.173205080756888,-0.8,-0.3));
#9572=CARTESIAN_POINT('',(0.173205080756888,-1.28,-0.3));
#9573=CARTESIAN_POINT('Origin',(-0.346410161513775,-0.8,-5.55111512312578E-17));
#9574=CARTESIAN_POINT('',(-0.346410161513775,-0.8,-4.24230095489963E-17));
#9575=CARTESIAN_POINT('',(-0.173205080756888,-0.8,-0.3));
#9576=CARTESIAN_POINT('',(-0.346410161513775,-1.28,-5.55111512312578E-17));
#9577=CARTESIAN_POINT('',(-0.346410161513775,-0.8,-4.24230095489963E-17));
#9578=CARTESIAN_POINT('',(-0.173205080756888,-1.28,-0.3));
#9579=CARTESIAN_POINT('Origin',(-0.173205080756888,-0.8,0.3));
#9580=CARTESIAN_POINT('',(-0.173205080756888,-0.8,0.3));
#9581=CARTESIAN_POINT('',(-0.346410161513775,-0.8,-4.24230095489963E-17));
#9582=CARTESIAN_POINT('',(-0.173205080756888,-1.28,0.3));
#9583=CARTESIAN_POINT('',(-0.173205080756888,-0.8,0.3));
#9584=CARTESIAN_POINT('',(-0.346410161513775,-1.28,-4.24230095489963E-17));
#9585=CARTESIAN_POINT('Origin',(0.173205080756888,-0.8,0.3));
#9586=CARTESIAN_POINT('',(0.173205080756888,-0.8,0.3));
#9587=CARTESIAN_POINT('',(-0.173205080756888,-0.8,0.3));
#9588=CARTESIAN_POINT('',(0.173205080756888,-1.28,0.3));
#9589=CARTESIAN_POINT('',(0.173205080756888,-0.8,0.3));
#9590=CARTESIAN_POINT('',(-0.173205080756888,-1.28,0.3));
#9591=CARTESIAN_POINT('Origin',(0.346410161513775,-0.8,0.));
#9592=CARTESIAN_POINT('',(0.173205080756888,-0.8,0.3));
#9593=CARTESIAN_POINT('',(0.173205080756888,-1.28,0.3));
#9594=CARTESIAN_POINT('Origin',(0.,-0.8,-5.55111512312578E-17));
#9595=CARTESIAN_POINT('Origin',(0.,-1.28,-5.55111512312578E-17));
#10048=UNCERTAINTY_MEASURE_WITH_UNIT(LENGTH_MEASURE(0.001),#10096,
'DISTANCE_ACCURACY_VALUE',
'Maximum model space distance between geometric entities at asserted c
onnectivities');
#10058=UNCERTAINTY_MEASURE_WITH_UNIT(LENGTH_MEASURE(0.001),#10096,
'DISTANCE_ACCURACY_VALUE',
'Maximum model space distance between geometric entities at asserted c
onnectivities');
#10085=(
GEOMETRIC_REPRESENTATION_CONTEXT(3)
GLOBAL_UNCERTAINTY_ASSIGNED_CONTEXT((#10048))
GLOBAL_UNIT_ASSIGNED_CONTEXT((#10096,#10098,#10099))
REPRESENTATION_CONTEXT('','3D')
);
#10095=(
GEOMETRIC_REPRESENTATION_CONTEXT(3)
GLOBAL_UNCERTAINTY_ASSIGNED_CONTEXT((#10058))
GLOBAL_UNIT_ASSIGNED_CONTEXT((#10096,#10098,#10099))
REPRESENTATION_CONTEXT('','3D')
);
#10096=(
LENGTH_UNIT()
NAMED_UNIT(*)
SI_UNIT(.CENTI.,.METRE.)
);
#10098=(
NAMED_UNIT(*)
PLANE_ANGLE_UNIT()
SI_UNIT($,.RADIAN.)
);
#10099=(
NAMED_UNIT(*)
SI_UNIT($,.STERADIAN.)
SOLID_ANGLE_UNIT()
);
#10126=SHAPE_DEFINITION_REPRESENTATION(#10197,#10273);
#10197=PRODUCT_DEFINITION_SHAPE('',$,#10310);
#10273=SHAPE_REPRESENTATION('',(#6425),#10085);
#10283=PRODUCT_DEFINITION_CONTEXT('part definition',#10393,'design');
#10310=PRODUCT_DEFINITION('Cap Screw - M8x30','Cap Screw - M8x30',#10346,
#10283);
#10346=PRODUCT_DEFINITION_FORMATION('',$,#10421);
#10393=APPLICATION_CONTEXT(
'Core Data for Automotive Mechanical Design Process');
#10394=PRODUCT_CONTEXT('part definition',#10393,'mechanical');
#10421=PRODUCT('Cap Screw - M8x30','Cap Screw - M8x30',
'Cap Screw - M8x30',(#10394));
#10501=COLOUR_RGB('Black',0.12,0.14,0.17);
#10502=FILL_AREA_STYLE_COLOUR('',#10501);
#10503=FILL_AREA_STYLE('',(#10502));
#10504=SURFACE_STYLE_FILL_AREA(#10503);
#10505=SURFACE_SIDE_STYLE('',(#10504));
#10506=SURFACE_STYLE_USAGE(.BOTH.,#10505);
#10507=PRESENTATION_STYLE_ASSIGNMENT((#10506));
ENDSEC;
END-ISO-10303-21;
